ISO-10303-21;
HEADER;
/* Generated by software containing ST-Developer
 * from STEP Tools, Inc. (www.steptools.com) 
 */

FILE_DESCRIPTION(
/* description */ ('Hand drill press frame (manual)'),
/* implementation_level */ '2;1');

FILE_NAME(
/* name */ 'Cap Screw - M4x16.step',
/* time_stamp */ '2026-10-28T03:25:28-07:00',
/* author */ (''),
/* organization */ (''),
/* preprocessor_version */ 'ST-DEVELOPER v20.2',
/* originating_system */ 'Autodesk Translation Framework v15.17.0.0',
/* authorisation */ '');

FILE_SCHEMA (('AUTOMOTIVE_DESIGN { 1 0 10303 214 3 1 1 }'));
ENDSEC;

DATA;
#10=MECHANICAL_DESIGN_GEOMETRIC_PRESENTATION_REPRESENTATION('',(#669),#33299);
#133=ORIENTED_CLOSED_SHELL('',*,#12690,.F.);
#136=BREP_WITH_VOIDS('Body1',#12689,(#133));
#487=CONICAL_SURFACE('',#14265,0.325,0.785398163397448);
#488=CONICAL_SURFACE('',#14269,0.335,0.785398163397448);
#489=CONICAL_SURFACE('',#14273,0.21,0.463647609000806);
#490=CONICAL_SURFACE('',#14277,0.18,0.785398163397448);
#572=SHAPE_REPRESENTATION_RELATIONSHIP('SRR','None',#33534,#617);
#617=ADVANCED_BREP_SHAPE_REPRESENTATION('',(#136),#33296);
#669=STYLED_ITEM('',(#33821),#136);
#884=FACE_BOUND('',#2865,.T.);
#1326=PLANE('',#14263);
#1327=PLANE('',#14271);
#1328=PLANE('',#14279);
#1329=PLANE('',#14280);
#1330=PLANE('',#14281);
#1331=PLANE('',#14282);
#1332=PLANE('',#14283);
#1333=PLANE('',#14284);
#1334=PLANE('',#14285);
#1335=PLANE('',#14286);
#1336=PLANE('',#14287);
#2007=FACE_OUTER_BOUND('',#2860,.T.);
#2008=FACE_OUTER_BOUND('',#2861,.T.);
#2009=FACE_OUTER_BOUND('',#2862,.T.);
#2010=FACE_OUTER_BOUND('',#2863,.T.);
#2011=FACE_OUTER_BOUND('',#2864,.T.);
#2012=FACE_OUTER_BOUND('',#2866,.T.);
#2013=FACE_OUTER_BOUND('',#2867,.T.);
#2014=FACE_OUTER_BOUND('',#2868,.T.);
#2015=FACE_OUTER_BOUND('',#2869,.T.);
#2016=FACE_OUTER_BOUND('',#2870,.T.);
#2017=FACE_OUTER_BOUND('',#2871,.T.);
#2018=FACE_OUTER_BOUND('',#2872,.T.);
#2019=FACE_OUTER_BOUND('',#2873,.T.);
#2020=FACE_OUTER_BOUND('',#2874,.T.);
#2021=FACE_OUTER_BOUND('',#2875,.T.);
#2022=FACE_OUTER_BOUND('',#2876,.T.);
#2023=FACE_OUTER_BOUND('',#2877,.T.);
#2860=EDGE_LOOP('',(#11709));
#2861=EDGE_LOOP('',(#11710,#11711,#11712,#11713));
#2862=EDGE_LOOP('',(#11714,#11715,#11716,#11717));
#2863=EDGE_LOOP('',(#11718,#11719,#11720,#11721));
#2864=EDGE_LOOP('',(#11722));
#2865=EDGE_LOOP('',(#11723));
#2866=EDGE_LOOP('',(#11724,#11725,#11726,#11727));
#2867=EDGE_LOOP('',(#11728,#11729,#11730,#11731));
#2868=EDGE_LOOP('',(#11732,#11733,#11734,#11735));
#2869=EDGE_LOOP('',(#11736));
#2870=EDGE_LOOP('',(#11737,#11738,#11739,#11740));
#2871=EDGE_LOOP('',(#11741,#11742,#11743,#11744));
#2872=EDGE_LOOP('',(#11745,#11746,#11747,#11748));
#2873=EDGE_LOOP('',(#11749,#11750,#11751,#11752));
#2874=EDGE_LOOP('',(#11753,#11754,#11755,#11756));
#2875=EDGE_LOOP('',(#11757,#11758,#11759,#11760));
#2876=EDGE_LOOP('',(#11761,#11762,#11763,#11764,#11765,#11766));
#2877=EDGE_LOOP('',(#11767,#11768,#11769,#11770,#11771,#11772));
#4023=LINE('',#33048,#5188);
#4024=LINE('',#33052,#5189);
#4025=LINE('',#33056,#5190);
#4026=LINE('',#33063,#5191);
#4027=LINE('',#33067,#5192);
#4028=LINE('',#33071,#5193);
#4029=LINE('',#33076,#5194);
#4030=LINE('',#33078,#5195);
#4031=LINE('',#33080,#5196);
#4032=LINE('',#33081,#5197);
#4033=LINE('',#33084,#5198);
#4034=LINE('',#33086,#5199);
#4035=LINE('',#33087,#5200);
#4036=LINE('',#33090,#5201);
#4037=LINE('',#33092,#5202);
#4038=LINE('',#33093,#5203);
#4039=LINE('',#33096,#5204);
#4040=LINE('',#33098,#5205);
#4041=LINE('',#33099,#5206);
#4042=LINE('',#33102,#5207);
#4043=LINE('',#33104,#5208);
#4044=LINE('',#33105,#5209);
#4045=LINE('',#33107,#5210);
#4046=LINE('',#33108,#5211);
#5188=VECTOR('',#17664,0.325);
#5189=VECTOR('',#17669,0.35);
#5190=VECTOR('',#17674,0.335);
#5191=VECTOR('',#17683,0.21);
#5192=VECTOR('',#17688,0.2);
#5193=VECTOR('',#17693,0.18);
#5194=VECTOR('',#17698,1.);
#5195=VECTOR('',#17699,1.);
#5196=VECTOR('',#17700,1.);
#5197=VECTOR('',#17701,1.);
#5198=VECTOR('',#17704,1.);
#5199=VECTOR('',#17705,1.);
#5200=VECTOR('',#17706,1.);
#5201=VECTOR('',#17709,1.);
#5202=VECTOR('',#17710,1.);
#5203=VECTOR('',#17711,1.);
#5204=VECTOR('',#17714,1.);
#5205=VECTOR('',#17715,1.);
#5206=VECTOR('',#17716,1.);
#5207=VECTOR('',#17719,1.);
#5208=VECTOR('',#17720,1.);
#5209=VECTOR('',#17721,1.);
#5210=VECTOR('',#17724,1.);
#5211=VECTOR('',#17725,1.);
#5601=CIRCLE('',#14264,0.3);
#5602=CIRCLE('',#14266,0.35);
#5603=CIRCLE('',#14268,0.35);
#5604=CIRCLE('',#14270,0.32);
#5605=CIRCLE('',#14272,0.22);
#5606=CIRCLE('',#14274,0.1954);
#5607=CIRCLE('',#14276,0.1954);
#5608=CIRCLE('',#14278,0.16);
#6715=VERTEX_POINT('',#33043);
#6716=VERTEX_POINT('',#33046);
#6717=VERTEX_POINT('',#33050);
#6718=VERTEX_POINT('',#33054);
#6719=VERTEX_POINT('',#33058);
#6720=VERTEX_POINT('',#33061);
#6721=VERTEX_POINT('',#33065);
#6722=VERTEX_POINT('',#33069);
#6723=VERTEX_POINT('',#33074);
#6724=VERTEX_POINT('',#33075);
#6725=VERTEX_POINT('',#33077);
#6726=VERTEX_POINT('',#33079);
#6727=VERTEX_POINT('',#33083);
#6728=VERTEX_POINT('',#33085);
#6729=VERTEX_POINT('',#33089);
#6730=VERTEX_POINT('',#33091);
#6731=VERTEX_POINT('',#33095);
#6732=VERTEX_POINT('',#33097);
#6733=VERTEX_POINT('',#33101);
#6734=VERTEX_POINT('',#33103);
#8383=EDGE_CURVE('',#6715,#6715,#5601,.T.);
#8384=EDGE_CURVE('',#6716,#6716,#5602,.T.);
#8385=EDGE_CURVE('',#6716,#6715,#4023,.T.);
#8386=EDGE_CURVE('',#6717,#6717,#5603,.T.);
#8387=EDGE_CURVE('',#6717,#6716,#4024,.T.);
#8388=EDGE_CURVE('',#6718,#6718,#5604,.T.);
#8389=EDGE_CURVE('',#6718,#6717,#4025,.T.);
#8390=EDGE_CURVE('',#6719,#6719,#5605,.T.);
#8391=EDGE_CURVE('',#6720,#6720,#5606,.F.);
#8392=EDGE_CURVE('',#6720,#6719,#4026,.T.);
#8393=EDGE_CURVE('',#6721,#6721,#5607,.F.);
#8394=EDGE_CURVE('',#6721,#6720,#4027,.T.);
#8395=EDGE_CURVE('',#6722,#6722,#5608,.T.);
#8396=EDGE_CURVE('',#6722,#6721,#4028,.T.);
#8397=EDGE_CURVE('',#6723,#6724,#4029,.T.);
#8398=EDGE_CURVE('',#6724,#6725,#4030,.T.);
#8399=EDGE_CURVE('',#6725,#6726,#4031,.T.);
#8400=EDGE_CURVE('',#6723,#6726,#4032,.T.);
#8401=EDGE_CURVE('',#6724,#6727,#4033,.T.);
#8402=EDGE_CURVE('',#6727,#6728,#4034,.T.);
#8403=EDGE_CURVE('',#6728,#6725,#4035,.T.);
#8404=EDGE_CURVE('',#6727,#6729,#4036,.T.);
#8405=EDGE_CURVE('',#6729,#6730,#4037,.T.);
#8406=EDGE_CURVE('',#6730,#6728,#4038,.T.);
#8407=EDGE_CURVE('',#6729,#6731,#4039,.T.);
#8408=EDGE_CURVE('',#6731,#6732,#4040,.T.);
#8409=EDGE_CURVE('',#6732,#6730,#4041,.T.);
#8410=EDGE_CURVE('',#6731,#6733,#4042,.T.);
#8411=EDGE_CURVE('',#6733,#6734,#4043,.T.);
#8412=EDGE_CURVE('',#6734,#6732,#4044,.T.);
#8413=EDGE_CURVE('',#6733,#6723,#4045,.T.);
#8414=EDGE_CURVE('',#6726,#6734,#4046,.T.);
#11709=ORIENTED_EDGE('',*,*,#8383,.F.);
#11710=ORIENTED_EDGE('',*,*,#8384,.F.);
#11711=ORIENTED_EDGE('',*,*,#8385,.T.);
#11712=ORIENTED_EDGE('',*,*,#8383,.T.);
#11713=ORIENTED_EDGE('',*,*,#8385,.F.);
#11714=ORIENTED_EDGE('',*,*,#8386,.F.);
#11715=ORIENTED_EDGE('',*,*,#8387,.T.);
#11716=ORIENTED_EDGE('',*,*,#8384,.T.);
#11717=ORIENTED_EDGE('',*,*,#8387,.F.);
#11718=ORIENTED_EDGE('',*,*,#8388,.F.);
#11719=ORIENTED_EDGE('',*,*,#8389,.T.);
#11720=ORIENTED_EDGE('',*,*,#8386,.T.);
#11721=ORIENTED_EDGE('',*,*,#8389,.F.);
#11722=ORIENTED_EDGE('',*,*,#8388,.T.);
#11723=ORIENTED_EDGE('',*,*,#8390,.F.);
#11724=ORIENTED_EDGE('',*,*,#8391,.F.);
#11725=ORIENTED_EDGE('',*,*,#8392,.T.);
#11726=ORIENTED_EDGE('',*,*,#8390,.T.);
#11727=ORIENTED_EDGE('',*,*,#8392,.F.);
#11728=ORIENTED_EDGE('',*,*,#8393,.F.);
#11729=ORIENTED_EDGE('',*,*,#8394,.T.);
#11730=ORIENTED_EDGE('',*,*,#8391,.T.);
#11731=ORIENTED_EDGE('',*,*,#8394,.F.);
#11732=ORIENTED_EDGE('',*,*,#8395,.F.);
#11733=ORIENTED_EDGE('',*,*,#8396,.T.);
#11734=ORIENTED_EDGE('',*,*,#8393,.T.);
#11735=ORIENTED_EDGE('',*,*,#8396,.F.);
#11736=ORIENTED_EDGE('',*,*,#8395,.T.);
#11737=ORIENTED_EDGE('',*,*,#8397,.T.);
#11738=ORIENTED_EDGE('',*,*,#8398,.T.);
#11739=ORIENTED_EDGE('',*,*,#8399,.T.);
#11740=ORIENTED_EDGE('',*,*,#8400,.F.);
#11741=ORIENTED_EDGE('',*,*,#8401,.T.);
#11742=ORIENTED_EDGE('',*,*,#8402,.T.);
#11743=ORIENTED_EDGE('',*,*,#8403,.T.);
#11744=ORIENTED_EDGE('',*,*,#8398,.F.);
#11745=ORIENTED_EDGE('',*,*,#8404,.T.);
#11746=ORIENTED_EDGE('',*,*,#8405,.T.);
#11747=ORIENTED_EDGE('',*,*,#8406,.T.);
#11748=ORIENTED_EDGE('',*,*,#8402,.F.);
#11749=ORIENTED_EDGE('',*,*,#8407,.T.);
#11750=ORIENTED_EDGE('',*,*,#8408,.T.);
#11751=ORIENTED_EDGE('',*,*,#8409,.T.);
#11752=ORIENTED_EDGE('',*,*,#8405,.F.);
#11753=ORIENTED_EDGE('',*,*,#8410,.T.);
#11754=ORIENTED_EDGE('',*,*,#8411,.T.);
#11755=ORIENTED_EDGE('',*,*,#8412,.T.);
#11756=ORIENTED_EDGE('',*,*,#8408,.F.);
#11757=ORIENTED_EDGE('',*,*,#8413,.T.);
#11758=ORIENTED_EDGE('',*,*,#8400,.T.);
#11759=ORIENTED_EDGE('',*,*,#8414,.T.);
#11760=ORIENTED_EDGE('',*,*,#8411,.F.);
#11761=ORIENTED_EDGE('',*,*,#8413,.F.);
#11762=ORIENTED_EDGE('',*,*,#8410,.F.);
#11763=ORIENTED_EDGE('',*,*,#8407,.F.);
#11764=ORIENTED_EDGE('',*,*,#8404,.F.);
#11765=ORIENTED_EDGE('',*,*,#8401,.F.);
#11766=ORIENTED_EDGE('',*,*,#8397,.F.);
#11767=ORIENTED_EDGE('',*,*,#8414,.F.);
#11768=ORIENTED_EDGE('',*,*,#8399,.F.);
#11769=ORIENTED_EDGE('',*,*,#8403,.F.);
#11770=ORIENTED_EDGE('',*,*,#8406,.F.);
#11771=ORIENTED_EDGE('',*,*,#8409,.F.);
#11772=ORIENTED_EDGE('',*,*,#8412,.F.);
#11944=CYLINDRICAL_SURFACE('',#14267,0.35);
#11945=CYLINDRICAL_SURFACE('',#14275,0.1954);
#12616=ADVANCED_FACE('',(#2007),#1326,.T.);
#12617=ADVANCED_FACE('',(#2008),#487,.T.);
#12618=ADVANCED_FACE('',(#2009),#11944,.T.);
#12619=ADVANCED_FACE('',(#2010),#488,.T.);
#12620=ADVANCED_FACE('',(#2011,#884),#1327,.T.);
#12621=ADVANCED_FACE('',(#2012),#489,.T.);
#12622=ADVANCED_FACE('',(#2013),#11945,.T.);
#12623=ADVANCED_FACE('',(#2014),#490,.T.);
#12624=ADVANCED_FACE('',(#2015),#1328,.T.);
#12625=ADVANCED_FACE('',(#2016),#1329,.F.);
#12626=ADVANCED_FACE('',(#2017),#1330,.F.);
#12627=ADVANCED_FACE('',(#2018),#1331,.F.);
#12628=ADVANCED_FACE('',(#2019),#1332,.F.);
#12629=ADVANCED_FACE('',(#2020),#1333,.F.);
#12630=ADVANCED_FACE('',(#2021),#1334,.F.);
#12631=ADVANCED_FACE('',(#2022),#1335,.F.);
#12632=ADVANCED_FACE('',(#2023),#1336,.F.);
#12689=CLOSED_SHELL('',(#12616,#12617,#12618,#12619,#12620,#12621,#12622,
#12623,#12624));
#12690=CLOSED_SHELL('',(#12625,#12626,#12627,#12628,#12629,#12630,#12631,
#12632));
#14262=AXIS2_PLACEMENT_3D('',#33041,#17654,#17655);
#14263=AXIS2_PLACEMENT_3D('',#33042,#17656,#17657);
#14264=AXIS2_PLACEMENT_3D('',#33044,#17658,#17659);
#14265=AXIS2_PLACEMENT_3D('',#33045,#17660,#17661);
#14266=AXIS2_PLACEMENT_3D('',#33047,#17662,#17663);
#14267=AXIS2_PLACEMENT_3D('',#33049,#17665,#17666);
#14268=AXIS2_PLACEMENT_3D('',#33051,#17667,#17668);
#14269=AXIS2_PLACEMENT_3D('',#33053,#17670,#17671);
#14270=AXIS2_PLACEMENT_3D('',#33055,#17672,#17673);
#14271=AXIS2_PLACEMENT_3D('',#33057,#17675,#17676);
#14272=AXIS2_PLACEMENT_3D('',#33059,#17677,#17678);
#14273=AXIS2_PLACEMENT_3D('',#33060,#17679,#17680);
#14274=AXIS2_PLACEMENT_3D('',#33062,#17681,#17682);
#14275=AXIS2_PLACEMENT_3D('',#33064,#17684,#17685);
#14276=AXIS2_PLACEMENT_3D('',#33066,#17686,#17687);
#14277=AXIS2_PLACEMENT_3D('',#33068,#17689,#17690);
#14278=AXIS2_PLACEMENT_3D('',#33070,#17691,#17692);
#14279=AXIS2_PLACEMENT_3D('',#33072,#17694,#17695);
#14280=AXIS2_PLACEMENT_3D('',#33073,#17696,#17697);
#14281=AXIS2_PLACEMENT_3D('',#33082,#17702,#17703);
#14282=AXIS2_PLACEMENT_3D('',#33088,#17707,#17708);
#14283=AXIS2_PLACEMENT_3D('',#33094,#17712,#17713);
#14284=AXIS2_PLACEMENT_3D('',#33100,#17717,#17718);
#14285=AXIS2_PLACEMENT_3D('',#33106,#17722,#17723);
#14286=AXIS2_PLACEMENT_3D('',#33109,#17726,#17727);
#14287=AXIS2_PLACEMENT_3D('',#33110,#17728,#17729);
#17654=DIRECTION('axis',(0.,0.,1.));
#17655=DIRECTION('refdir',(1.,0.,0.));
#17656=DIRECTION('center_axis',(0.,1.,0.));
#17657=DIRECTION('ref_axis',(0.,0.,1.));
#17658=DIRECTION('center_axis',(0.,-1.,0.));
#17659=DIRECTION('ref_axis',(1.,0.,0.));
#17660=DIRECTION('center_axis',(0.,-1.,0.));
#17661=DIRECTION('ref_axis',(1.,0.,0.));
#17662=DIRECTION('center_axis',(0.,-1.,0.));
#17663=DIRECTION('ref_axis',(1.,0.,0.));
#17664=DIRECTION('',(0.707106781186547,0.707106781186548,8.65956056235493E-17));
#17665=DIRECTION('center_axis',(0.,-1.,0.));
#17666=DIRECTION('ref_axis',(1.,0.,0.));
#17667=DIRECTION('center_axis',(0.,-1.,0.));
#17668=DIRECTION('ref_axis',(1.,0.,0.));
#17669=DIRECTION('',(0.,1.,0.));
#17670=DIRECTION('center_axis',(0.,1.,0.));
#17671=DIRECTION('ref_axis',(1.,0.,0.));
#17672=DIRECTION('center_axis',(0.,-1.,0.));
#17673=DIRECTION('ref_axis',(1.,0.,0.));
#17674=DIRECTION('',(-0.707106781186547,0.707106781186548,-8.65956056235493E-17));
#17675=DIRECTION('center_axis',(0.,-1.,0.));
#17676=DIRECTION('ref_axis',(0.,0.,-1.));
#17677=DIRECTION('center_axis',(0.,-1.,0.));
#17678=DIRECTION('ref_axis',(1.,0.,0.));
#17679=DIRECTION('center_axis',(0.,1.,0.));
#17680=DIRECTION('ref_axis',(1.,0.,0.));
#17681=DIRECTION('center_axis',(0.,1.,0.));
#17682=DIRECTION('ref_axis',(1.,0.,0.));
#17683=DIRECTION('',(-0.447213595499958,0.894427190999916,-5.47678698264203E-17));
#17684=DIRECTION('center_axis',(0.,-1.,0.));
#17685=DIRECTION('ref_axis',(1.,0.,0.));
#17686=DIRECTION('center_axis',(0.,1.,0.));
#17687=DIRECTION('ref_axis',(1.,0.,0.));
#17688=DIRECTION('',(0.,1.,0.));
#17689=DIRECTION('center_axis',(0.,1.,0.));
#17690=DIRECTION('ref_axis',(1.,0.,0.));
#17691=DIRECTION('center_axis',(0.,-1.,0.));
#17692=DIRECTION('ref_axis',(1.,0.,0.));
#17693=DIRECTION('',(-0.707106781186547,0.707106781186548,-8.65956056235493E-17));
#17694=DIRECTION('center_axis',(0.,-1.,0.));
#17695=DIRECTION('ref_axis',(0.,0.,-1.));
#17696=DIRECTION('center_axis',(0.866025403784439,0.,-0.5));
#17697=DIRECTION('ref_axis',(0.5,0.,0.866025403784439));
#17698=DIRECTION('',(-0.5,0.,-0.866025403784439));
#17699=DIRECTION('',(0.,-1.,0.));
#17700=DIRECTION('',(0.5,0.,0.866025403784439));
#17701=DIRECTION('',(0.,-1.,0.));
#17702=DIRECTION('center_axis',(1.60246890531964E-16,0.,-1.));
#17703=DIRECTION('ref_axis',(1.,0.,1.60246890531964E-16));
#17704=DIRECTION('',(-1.,0.,-1.60246890531964E-16));
#17705=DIRECTION('',(0.,-1.,0.));
#17706=DIRECTION('',(1.,0.,1.60246890531964E-16));
#17707=DIRECTION('center_axis',(-0.866025403784439,0.,-0.5));
#17708=DIRECTION('ref_axis',(0.5,0.,-0.866025403784439));
#17709=DIRECTION('',(-0.5,0.,0.866025403784439));
#17710=DIRECTION('',(0.,-1.,0.));
#17711=DIRECTION('',(0.5,0.,-0.866025403784439));
#17712=DIRECTION('center_axis',(-0.866025403784439,0.,0.5));
#17713=DIRECTION('ref_axis',(-0.5,0.,-0.866025403784439));
#17714=DIRECTION('',(0.5,0.,0.866025403784439));
#17715=DIRECTION('',(0.,-1.,0.));
#17716=DIRECTION('',(-0.5,0.,-0.866025403784439));
#17717=DIRECTION('center_axis',(-1.60246890531964E-16,0.,1.));
#17718=DIRECTION('ref_axis',(-1.,0.,-1.60246890531964E-16));
#17719=DIRECTION('',(1.,0.,1.60246890531964E-16));
#17720=DIRECTION('',(0.,-1.,0.));
#17721=DIRECTION('',(-1.,0.,-1.60246890531964E-16));
#17722=DIRECTION('center_axis',(0.866025403784439,0.,0.5));
#17723=DIRECTION('ref_axis',(-0.5,0.,0.866025403784439));
#17724=DIRECTION('',(0.5,0.,-0.866025403784439));
#17725=DIRECTION('',(-0.5,0.,0.866025403784439));
#17726=DIRECTION('center_axis',(0.,1.,0.));
#17727=DIRECTION('ref_axis',(1.,0.,0.));
#17728=DIRECTION('center_axis',(0.,-1.,0.));
#17729=DIRECTION('ref_axis',(0.,0.,-1.));
#33041=CARTESIAN_POINT('',(0.,0.,0.));
#33042=CARTESIAN_POINT('Origin',(0.3,0.4,0.));
#33043=CARTESIAN_POINT('',(-0.3,0.4,-3.67394039744206E-17));
#33044=CARTESIAN_POINT('Origin',(0.,0.4,0.));
#33045=CARTESIAN_POINT('Origin',(0.,0.375,0.));
#33046=CARTESIAN_POINT('',(-0.35,0.35,-4.28626379701573E-17));
#33047=CARTESIAN_POINT('Origin',(0.,0.35,0.));
#33048=CARTESIAN_POINT('',(-0.325,0.375,-3.9801020972289E-17));
#33049=CARTESIAN_POINT('Origin',(0.,0.19,0.));
#33050=CARTESIAN_POINT('',(-0.35,0.03,-4.28626379701574E-17));
#33051=CARTESIAN_POINT('Origin',(0.,0.03,0.));
#33052=CARTESIAN_POINT('',(-0.35,0.19,-4.28626379701574E-17));
#33053=CARTESIAN_POINT('Origin',(0.,0.0149999999999999,0.));
#33054=CARTESIAN_POINT('',(-0.32,-3.29597460435593E-17,-3.91886975727153E-17));
#33055=CARTESIAN_POINT('Origin',(0.,0.,0.));
#33056=CARTESIAN_POINT('',(-0.335,0.0149999999999999,-4.10256677714363E-17));
#33057=CARTESIAN_POINT('Origin',(0.22,0.,0.));
#33058=CARTESIAN_POINT('',(-0.22,-6.93889390390723E-18,-2.69422295812418E-17));
#33059=CARTESIAN_POINT('Origin',(0.,0.,0.));
#33060=CARTESIAN_POINT('Origin',(0.,-0.02,0.));
#33061=CARTESIAN_POINT('',(-0.1954,-0.0492,2.39295984553393E-17));
#33062=CARTESIAN_POINT('Origin',(0.,-0.0492,0.));
#33063=CARTESIAN_POINT('',(-0.21,-0.02,-2.57175827820944E-17));
#33064=CARTESIAN_POINT('Origin',(0.,-0.8,0.));
#33065=CARTESIAN_POINT('',(-0.1954,-1.5646,2.39295984553393E-17));
#33066=CARTESIAN_POINT('Origin',(0.,-1.5646,0.));
#33067=CARTESIAN_POINT('',(-0.1954,-0.8,-2.39295984553393E-17));
#33068=CARTESIAN_POINT('Origin',(0.,-1.58,0.));
#33069=CARTESIAN_POINT('',(-0.16,-1.6,-1.95943487863577E-17));
#33070=CARTESIAN_POINT('Origin',(0.,-1.6,0.));
#33071=CARTESIAN_POINT('',(-0.18,-1.58,-2.20436423846524E-17));
#33072=CARTESIAN_POINT('Origin',(0.,-1.6,0.));
#33073=CARTESIAN_POINT('Origin',(0.0866025403784439,-0.4,-0.15));
#33074=CARTESIAN_POINT('',(0.173205080756888,-0.4,0.));
#33075=CARTESIAN_POINT('',(0.0866025403784439,-0.4,-0.15));
#33076=CARTESIAN_POINT('',(0.173205080756888,-0.4,0.));
#33077=CARTESIAN_POINT('',(0.0866025403784439,-0.64,-0.15));
#33078=CARTESIAN_POINT('',(0.0866025403784439,-0.4,-0.15));
#33079=CARTESIAN_POINT('',(0.173205080756888,-0.64,0.));
#33080=CARTESIAN_POINT('',(0.173205080756888,-0.64,0.));
#33081=CARTESIAN_POINT('',(0.173205080756888,-0.4,0.));
#33082=CARTESIAN_POINT('Origin',(-0.0866025403784438,-0.4,-0.15));
#33083=CARTESIAN_POINT('',(-0.0866025403784438,-0.4,-0.15));
#33084=CARTESIAN_POINT('',(0.0866025403784439,-0.4,-0.15));
#33085=CARTESIAN_POINT('',(-0.0866025403784438,-0.64,-0.15));
#33086=CARTESIAN_POINT('',(-0.0866025403784438,-0.4,-0.15));
#33087=CARTESIAN_POINT('',(0.0866025403784439,-0.64,-0.15));
#33088=CARTESIAN_POINT('Origin',(-0.173205080756888,-0.4,-2.77555756156289E-17));
#33089=CARTESIAN_POINT('',(-0.173205080756888,-0.4,-2.12115047744981E-17));
#33090=CARTESIAN_POINT('',(-0.0866025403784438,-0.4,-0.15));
#33091=CARTESIAN_POINT('',(-0.173205080756888,-0.64,-2.77555756156289E-17));
#33092=CARTESIAN_POINT('',(-0.173205080756888,-0.4,-2.12115047744981E-17));
#33093=CARTESIAN_POINT('',(-0.0866025403784438,-0.64,-0.15));
#33094=CARTESIAN_POINT('Origin',(-0.0866025403784439,-0.4,0.15));
#33095=CARTESIAN_POINT('',(-0.0866025403784439,-0.4,0.15));
#33096=CARTESIAN_POINT('',(-0.173205080756888,-0.4,-2.12115047744981E-17));
#33097=CARTESIAN_POINT('',(-0.0866025403784439,-0.64,0.15));
#33098=CARTESIAN_POINT('',(-0.0866025403784439,-0.4,0.15));
#33099=CARTESIAN_POINT('',(-0.173205080756888,-0.64,-2.12115047744981E-17));
#33100=CARTESIAN_POINT('Origin',(0.0866025403784439,-0.4,0.15));
#33101=CARTESIAN_POINT('',(0.0866025403784439,-0.4,0.15));
#33102=CARTESIAN_POINT('',(-0.0866025403784439,-0.4,0.15));
#33103=CARTESIAN_POINT('',(0.0866025403784439,-0.64,0.15));
#33104=CARTESIAN_POINT('',(0.0866025403784439,-0.4,0.15));
#33105=CARTESIAN_POINT('',(-0.0866025403784439,-0.64,0.15));
#33106=CARTESIAN_POINT('Origin',(0.173205080756888,-0.4,0.));
#33107=CARTESIAN_POINT('',(0.0866025403784439,-0.4,0.15));
#33108=CARTESIAN_POINT('',(0.0866025403784439,-0.64,0.15));
#33109=CARTESIAN_POINT('Origin',(0.,-0.4,-2.77555756156289E-17));
#33110=CARTESIAN_POINT('Origin',(0.,-0.64,-2.77555756156289E-17));
#33244=UNCERTAINTY_MEASURE_WITH_UNIT(LENGTH_MEASURE(0.001),#33300,
'DISTANCE_ACCURACY_VALUE',
'Maximum model space distance between geometric entities at asserted c
onnectivities');
#33247=UNCERTAINTY_MEASURE_WITH_UNIT(LENGTH_MEASURE(0.001),#33300,
'DISTANCE_ACCURACY_VALUE',
'Maximum model space distance between geometric entities at asserted c
onnectivities');
#33296=(
GEOMETRIC_REPRESENTATION_CONTEXT(3)
GLOBAL_UNCERTAINTY_ASSIGNED_CONTEXT((#33244))
GLOBAL_UNIT_ASSIGNED_CONTEXT((#33300,#33302,#33303))
REPRESENTATION_CONTEXT('','3D')
);
#33299=(
GEOMETRIC_REPRESENTATION_CONTEXT(3)
GLOBAL_UNCERTAINTY_ASSIGNED_CONTEXT((#33247))
GLOBAL_UNIT_ASSIGNED_CONTEXT((#33300,#33302,#33303))
REPRESENTATION_CONTEXT('','3D')
);
#33300=(
LENGTH_UNIT()
NAMED_UNIT(*)
SI_UNIT(.CENTI.,.METRE.)
);
#33302=(
NAMED_UNIT(*)
PLANE_ANGLE_UNIT()
SI_UNIT($,.RADIAN.)
);
#33303=(
NAMED_UNIT(*)
SI_UNIT($,.STERADIAN.)
SOLID_ANGLE_UNIT()
);
#33352=SHAPE_DEFINITION_REPRESENTATION(#33414,#33534);
#33414=PRODUCT_DEFINITION_SHAPE('',$,#33586);
#33534=SHAPE_REPRESENTATION('',(#14262),#33296);
#33537=PRODUCT_DEFINITION_CONTEXT('part definition',#33692,'design');
#33586=PRODUCT_DEFINITION('Cap Screw - M4x16','Cap Screw - M4x16',#33637,
#33537);
#33637=PRODUCT_DEFINITION_FORMATION('',$,#33742);
#33692=APPLICATION_CONTEXT(
'Core Data for Automotive Mechanical Design Process');
#33693=PRODUCT_CONTEXT('part definition',#33692,'mechanical');
#33742=PRODUCT('Cap Screw - M4x16','Cap Screw - M4x16',
'Cap Screw - M4x16',(#33693));
#33815=COLOUR_RGB('Black',0.12,0.14,0.17);
#33816=FILL_AREA_STYLE_COLOUR('',#33815);
#33817=FILL_AREA_STYLE('',(#33816));
#33818=SURFACE_STYLE_FILL_AREA(#33817);
#33819=SURFACE_SIDE_STYLE('',(#33818));
#33820=SURFACE_STYLE_USAGE(.BOTH.,#33819);
#33821=PRESENTATION_STYLE_ASSIGNMENT((#33820));
ENDSEC;
END-ISO-10303-21;
